ISO-10303-21;
HEADER;
/* Generated by software containing ST-Developer
 * from STEP Tools, Inc. (www.steptools.com) 
 */

FILE_DESCRIPTION(
/* description */ ('Belt tension measurement rig'),
/* implementation_level */ '2;1');

FILE_NAME(
/* name */ 'M5x14 Cap Screw.step',
/* time_stamp */ '2026-10-28T03:24:44-07:00',
/* author */ (''),
/* organization */ (''),
/* preprocessor_version */ 'ST-DEVELOPER v20.2',
/* originating_system */ 'Autodesk Translation Framework v15.17.0.0',
/* authorisation */ '');

FILE_SCHEMA (('AUTOMOTIVE_DESIGN { 1 0 10303 214 3 1 1 }'));
ENDSEC;

DATA;
#10=MECHANICAL_DESIGN_GEOMETRIC_PRESENTATION_REPRESENTATION('',(#730),#23587);
#11=ORIENTED_CLOSED_SHELL('',*,#12235,.F.);
#14=BREP_WITH_VOIDS('Body1',#12236,(#11));
#471=CONICAL_SURFACE('',#13642,0.4,0.785398163397448);
#472=CONICAL_SURFACE('',#13646,0.41,0.785398163397448);
#473=CONICAL_SURFACE('',#13650,0.26,0.463647609000806);
#612=SHAPE_REPRESENTATION_RELATIONSHIP('SRR','None',#23860,#667);
#667=ADVANCED_BREP_SHAPE_REPRESENTATION('',(#14),#23558);
#730=STYLED_ITEM('',(#24218),#14);
#973=FACE_BOUND('',#2581,.T.);
#1239=PLANE('',#13630);
#1240=PLANE('',#13631);
#1241=PLANE('',#13632);
#1242=PLANE('',#13633);
#1243=PLANE('',#13634);
#1244=PLANE('',#13635);
#1245=PLANE('',#13636);
#1246=PLANE('',#13637);
#1247=PLANE('',#13638);
#1248=PLANE('',#13640);
#1249=PLANE('',#13648);
#1719=FACE_OUTER_BOUND('',#2567,.T.);
#1720=FACE_OUTER_BOUND('',#2568,.T.);
#1721=FACE_OUTER_BOUND('',#2569,.T.);
#1722=FACE_OUTER_BOUND('',#2570,.T.);
#1723=FACE_OUTER_BOUND('',#2571,.T.);
#1724=FACE_OUTER_BOUND('',#2572,.T.);
#1725=FACE_OUTER_BOUND('',#2573,.T.);
#1726=FACE_OUTER_BOUND('',#2574,.T.);
#1727=FACE_OUTER_BOUND('',#2575,.T.);
#1728=FACE_OUTER_BOUND('',#2576,.T.);
#1729=FACE_OUTER_BOUND('',#2577,.T.);
#1730=FACE_OUTER_BOUND('',#2578,.T.);
#1731=FACE_OUTER_BOUND('',#2579,.T.);
#1732=FACE_OUTER_BOUND('',#2580,.T.);
#1733=FACE_OUTER_BOUND('',#2582,.T.);
#1734=FACE_OUTER_BOUND('',#2583,.T.);
#2567=EDGE_LOOP('',(#9602,#9603,#9604,#9605));
#2568=EDGE_LOOP('',(#9606,#9607,#9608,#9609));
#2569=EDGE_LOOP('',(#9610,#9611,#9612,#9613));
#2570=EDGE_LOOP('',(#9614,#9615,#9616,#9617));
#2571=EDGE_LOOP('',(#9618,#9619,#9620,#9621));
#2572=EDGE_LOOP('',(#9622,#9623,#9624,#9625));
#2573=EDGE_LOOP('',(#9626,#9627,#9628,#9629,#9630,#9631));
#2574=EDGE_LOOP('',(#9632,#9633,#9634,#9635,#9636,#9637));
#2575=EDGE_LOOP('',(#9638));
#2576=EDGE_LOOP('',(#9639));
#2577=EDGE_LOOP('',(#9640,#9641,#9642,#9643));
#2578=EDGE_LOOP('',(#9644,#9645,#9646,#9647));
#2579=EDGE_LOOP('',(#9648,#9649,#9650,#9651));
#2580=EDGE_LOOP('',(#9652));
#2581=EDGE_LOOP('',(#9653));
#2582=EDGE_LOOP('',(#9654,#9655,#9656,#9657));
#2583=EDGE_LOOP('',(#9658,#9659,#9660,#9661));
#3431=LINE('',#20787,#4182);
#3432=LINE('',#20789,#4183);
#3433=LINE('',#20791,#4184);
#3434=LINE('',#20792,#4185);
#3435=LINE('',#20795,#4186);
#3436=LINE('',#20797,#4187);
#3437=LINE('',#20798,#4188);
#3438=LINE('',#20801,#4189);
#3439=LINE('',#20803,#4190);
#3440=LINE('',#20804,#4191);
#3441=LINE('',#20807,#4192);
#3442=LINE('',#20809,#4193);
#3443=LINE('',#20810,#4194);
#3444=LINE('',#20813,#4195);
#3445=LINE('',#20815,#4196);
#3446=LINE('',#20816,#4197);
#3447=LINE('',#20818,#4198);
#3448=LINE('',#20819,#4199);
#3449=LINE('',#20831,#4200);
#3450=LINE('',#20835,#4201);
#3451=LINE('',#20839,#4202);
#3452=LINE('',#20846,#4203);
#3453=LINE('',#20848,#4204);
#4182=VECTOR('',#16490,1.);
#4183=VECTOR('',#16491,1.);
#4184=VECTOR('',#16492,1.);
#4185=VECTOR('',#16493,1.);
#4186=VECTOR('',#16496,1.);
#4187=VECTOR('',#16497,1.);
#4188=VECTOR('',#16498,1.);
#4189=VECTOR('',#16501,1.);
#4190=VECTOR('',#16502,1.);
#4191=VECTOR('',#16503,1.);
#4192=VECTOR('',#16506,1.);
#4193=VECTOR('',#16507,1.);
#4194=VECTOR('',#16508,1.);
#4195=VECTOR('',#16511,1.);
#4196=VECTOR('',#16512,1.);
#4197=VECTOR('',#16513,1.);
#4198=VECTOR('',#16516,1.);
#4199=VECTOR('',#16517,1.);
#4200=VECTOR('',#16534,0.4);
#4201=VECTOR('',#16539,0.425);
#4202=VECTOR('',#16544,0.41);
#4203=VECTOR('',#16553,0.26);
#4204=VECTOR('',#16556,0.25);
#4813=CIRCLE('',#13639,0.24505);
#4814=CIRCLE('',#13641,0.375);
#4815=CIRCLE('',#13643,0.425);
#4816=CIRCLE('',#13645,0.425);
#4817=CIRCLE('',#13647,0.395);
#4818=CIRCLE('',#13649,0.27);
#4819=CIRCLE('',#13651,0.24505);
#5799=VERTEX_POINT('',#20785);
#5800=VERTEX_POINT('',#20786);
#5801=VERTEX_POINT('',#20788);
#5802=VERTEX_POINT('',#20790);
#5803=VERTEX_POINT('',#20794);
#5804=VERTEX_POINT('',#20796);
#5805=VERTEX_POINT('',#20800);
#5806=VERTEX_POINT('',#20802);
#5807=VERTEX_POINT('',#20806);
#5808=VERTEX_POINT('',#20808);
#5809=VERTEX_POINT('',#20812);
#5810=VERTEX_POINT('',#20814);
#5811=VERTEX_POINT('',#20823);
#5812=VERTEX_POINT('',#20826);
#5813=VERTEX_POINT('',#20829);
#5814=VERTEX_POINT('',#20833);
#5815=VERTEX_POINT('',#20837);
#5816=VERTEX_POINT('',#20841);
#5817=VERTEX_POINT('',#20844);
#7160=EDGE_CURVE('',#5799,#5800,#3431,.T.);
#7161=EDGE_CURVE('',#5800,#5801,#3432,.T.);
#7162=EDGE_CURVE('',#5801,#5802,#3433,.T.);
#7163=EDGE_CURVE('',#5799,#5802,#3434,.T.);
#7164=EDGE_CURVE('',#5800,#5803,#3435,.T.);
#7165=EDGE_CURVE('',#5803,#5804,#3436,.T.);
#7166=EDGE_CURVE('',#5804,#5801,#3437,.T.);
#7167=EDGE_CURVE('',#5803,#5805,#3438,.T.);
#7168=EDGE_CURVE('',#5805,#5806,#3439,.T.);
#7169=EDGE_CURVE('',#5806,#5804,#3440,.T.);
#7170=EDGE_CURVE('',#5805,#5807,#3441,.T.);
#7171=EDGE_CURVE('',#5807,#5808,#3442,.T.);
#7172=EDGE_CURVE('',#5808,#5806,#3443,.T.);
#7173=EDGE_CURVE('',#5807,#5809,#3444,.T.);
#7174=EDGE_CURVE('',#5809,#5810,#3445,.T.);
#7175=EDGE_CURVE('',#5810,#5808,#3446,.T.);
#7176=EDGE_CURVE('',#5809,#5799,#3447,.T.);
#7177=EDGE_CURVE('',#5802,#5810,#3448,.T.);
#7178=EDGE_CURVE('',#5811,#5811,#4813,.T.);
#7179=EDGE_CURVE('',#5812,#5812,#4814,.T.);
#7180=EDGE_CURVE('',#5813,#5813,#4815,.T.);
#7181=EDGE_CURVE('',#5813,#5812,#3449,.T.);
#7182=EDGE_CURVE('',#5814,#5814,#4816,.T.);
#7183=EDGE_CURVE('',#5814,#5813,#3450,.T.);
#7184=EDGE_CURVE('',#5815,#5815,#4817,.T.);
#7185=EDGE_CURVE('',#5815,#5814,#3451,.T.);
#7186=EDGE_CURVE('',#5816,#5816,#4818,.T.);
#7187=EDGE_CURVE('',#5817,#5817,#4819,.F.);
#7188=EDGE_CURVE('',#5817,#5816,#3452,.T.);
#7189=EDGE_CURVE('',#5811,#5817,#3453,.T.);
#9602=ORIENTED_EDGE('',*,*,#7160,.T.);
#9603=ORIENTED_EDGE('',*,*,#7161,.T.);
#9604=ORIENTED_EDGE('',*,*,#7162,.T.);
#9605=ORIENTED_EDGE('',*,*,#7163,.F.);
#9606=ORIENTED_EDGE('',*,*,#7164,.T.);
#9607=ORIENTED_EDGE('',*,*,#7165,.T.);
#9608=ORIENTED_EDGE('',*,*,#7166,.T.);
#9609=ORIENTED_EDGE('',*,*,#7161,.F.);
#9610=ORIENTED_EDGE('',*,*,#7167,.T.);
#9611=ORIENTED_EDGE('',*,*,#7168,.T.);
#9612=ORIENTED_EDGE('',*,*,#7169,.T.);
#9613=ORIENTED_EDGE('',*,*,#7165,.F.);
#9614=ORIENTED_EDGE('',*,*,#7170,.T.);
#9615=ORIENTED_EDGE('',*,*,#7171,.T.);
#9616=ORIENTED_EDGE('',*,*,#7172,.T.);
#9617=ORIENTED_EDGE('',*,*,#7168,.F.);
#9618=ORIENTED_EDGE('',*,*,#7173,.T.);
#9619=ORIENTED_EDGE('',*,*,#7174,.T.);
#9620=ORIENTED_EDGE('',*,*,#7175,.T.);
#9621=ORIENTED_EDGE('',*,*,#7171,.F.);
#9622=ORIENTED_EDGE('',*,*,#7176,.T.);
#9623=ORIENTED_EDGE('',*,*,#7163,.T.);
#9624=ORIENTED_EDGE('',*,*,#7177,.T.);
#9625=ORIENTED_EDGE('',*,*,#7174,.F.);
#9626=ORIENTED_EDGE('',*,*,#7176,.F.);
#9627=ORIENTED_EDGE('',*,*,#7173,.F.);
#9628=ORIENTED_EDGE('',*,*,#7170,.F.);
#9629=ORIENTED_EDGE('',*,*,#7167,.F.);
#9630=ORIENTED_EDGE('',*,*,#7164,.F.);
#9631=ORIENTED_EDGE('',*,*,#7160,.F.);
#9632=ORIENTED_EDGE('',*,*,#7177,.F.);
#9633=ORIENTED_EDGE('',*,*,#7162,.F.);
#9634=ORIENTED_EDGE('',*,*,#7166,.F.);
#9635=ORIENTED_EDGE('',*,*,#7169,.F.);
#9636=ORIENTED_EDGE('',*,*,#7172,.F.);
#9637=ORIENTED_EDGE('',*,*,#7175,.F.);
#9638=ORIENTED_EDGE('',*,*,#7178,.F.);
#9639=ORIENTED_EDGE('',*,*,#7179,.F.);
#9640=ORIENTED_EDGE('',*,*,#7180,.F.);
#9641=ORIENTED_EDGE('',*,*,#7181,.T.);
#9642=ORIENTED_EDGE('',*,*,#7179,.T.);
#9643=ORIENTED_EDGE('',*,*,#7181,.F.);
#9644=ORIENTED_EDGE('',*,*,#7182,.F.);
#9645=ORIENTED_EDGE('',*,*,#7183,.T.);
#9646=ORIENTED_EDGE('',*,*,#7180,.T.);
#9647=ORIENTED_EDGE('',*,*,#7183,.F.);
#9648=ORIENTED_EDGE('',*,*,#7184,.F.);
#9649=ORIENTED_EDGE('',*,*,#7185,.T.);
#9650=ORIENTED_EDGE('',*,*,#7182,.T.);
#9651=ORIENTED_EDGE('',*,*,#7185,.F.);
#9652=ORIENTED_EDGE('',*,*,#7184,.T.);
#9653=ORIENTED_EDGE('',*,*,#7186,.F.);
#9654=ORIENTED_EDGE('',*,*,#7187,.F.);
#9655=ORIENTED_EDGE('',*,*,#7188,.T.);
#9656=ORIENTED_EDGE('',*,*,#7186,.T.);
#9657=ORIENTED_EDGE('',*,*,#7188,.F.);
#9658=ORIENTED_EDGE('',*,*,#7178,.T.);
#9659=ORIENTED_EDGE('',*,*,#7189,.T.);
#9660=ORIENTED_EDGE('',*,*,#7187,.T.);
#9661=ORIENTED_EDGE('',*,*,#7189,.F.);
#11301=CYLINDRICAL_SURFACE('',#13644,0.425);
#11302=CYLINDRICAL_SURFACE('',#13652,0.24505);
#11860=ADVANCED_FACE('',(#1719),#1239,.F.);
#11861=ADVANCED_FACE('',(#1720),#1240,.F.);
#11862=ADVANCED_FACE('',(#1721),#1241,.F.);
#11863=ADVANCED_FACE('',(#1722),#1242,.F.);
#11864=ADVANCED_FACE('',(#1723),#1243,.F.);
#11865=ADVANCED_FACE('',(#1724),#1244,.F.);
#11866=ADVANCED_FACE('',(#1725),#1245,.F.);
#11867=ADVANCED_FACE('',(#1726),#1246,.F.);
#11868=ADVANCED_FACE('',(#1727),#1247,.F.);
#11869=ADVANCED_FACE('',(#1728),#1248,.T.);
#11870=ADVANCED_FACE('',(#1729),#471,.T.);
#11871=ADVANCED_FACE('',(#1730),#11301,.T.);
#11872=ADVANCED_FACE('',(#1731),#472,.T.);
#11873=ADVANCED_FACE('',(#1732,#973),#1249,.T.);
#11874=ADVANCED_FACE('',(#1733),#473,.T.);
#11875=ADVANCED_FACE('',(#1734),#11302,.T.);
#12235=CLOSED_SHELL('',(#11860,#11861,#11862,#11863,#11864,#11865,#11866,
#11867));
#12236=CLOSED_SHELL('',(#11868,#11869,#11870,#11871,#11872,#11873,#11874,
#11875));
#13629=AXIS2_PLACEMENT_3D('',#20783,#16486,#16487);
#13630=AXIS2_PLACEMENT_3D('',#20784,#16488,#16489);
#13631=AXIS2_PLACEMENT_3D('',#20793,#16494,#16495);
#13632=AXIS2_PLACEMENT_3D('',#20799,#16499,#16500);
#13633=AXIS2_PLACEMENT_3D('',#20805,#16504,#16505);
#13634=AXIS2_PLACEMENT_3D('',#20811,#16509,#16510);
#13635=AXIS2_PLACEMENT_3D('',#20817,#16514,#16515);
#13636=AXIS2_PLACEMENT_3D('',#20820,#16518,#16519);
#13637=AXIS2_PLACEMENT_3D('',#20821,#16520,#16521);
#13638=AXIS2_PLACEMENT_3D('',#20822,#16522,#16523);
#13639=AXIS2_PLACEMENT_3D('',#20824,#16524,#16525);
#13640=AXIS2_PLACEMENT_3D('',#20825,#16526,#16527);
#13641=AXIS2_PLACEMENT_3D('',#20827,#16528,#16529);
#13642=AXIS2_PLACEMENT_3D('',#20828,#16530,#16531);
#13643=AXIS2_PLACEMENT_3D('',#20830,#16532,#16533);
#13644=AXIS2_PLACEMENT_3D('',#20832,#16535,#16536);
#13645=AXIS2_PLACEMENT_3D('',#20834,#16537,#16538);
#13646=AXIS2_PLACEMENT_3D('',#20836,#16540,#16541);
#13647=AXIS2_PLACEMENT_3D('',#20838,#16542,#16543);
#13648=AXIS2_PLACEMENT_3D('',#20840,#16545,#16546);
#13649=AXIS2_PLACEMENT_3D('',#20842,#16547,#16548);
#13650=AXIS2_PLACEMENT_3D('',#20843,#16549,#16550);
#13651=AXIS2_PLACEMENT_3D('',#20845,#16551,#16552);
#13652=AXIS2_PLACEMENT_3D('',#20847,#16554,#16555);
#16486=DIRECTION('axis',(0.,0.,1.));
#16487=DIRECTION('refdir',(1.,0.,0.));
#16488=DIRECTION('center_axis',(0.866025403784439,0.,-0.5));
#16489=DIRECTION('ref_axis',(0.5,0.,0.866025403784439));
#16490=DIRECTION('',(-0.5,0.,-0.866025403784439));
#16491=DIRECTION('',(0.,-1.,0.));
#16492=DIRECTION('',(0.5,0.,0.866025403784439));
#16493=DIRECTION('',(0.,-1.,0.));
#16494=DIRECTION('center_axis',(1.20185167898973E-16,0.,-1.));
#16495=DIRECTION('ref_axis',(1.,0.,1.20185167898973E-16));
#16496=DIRECTION('',(-1.,0.,-1.20185167898973E-16));
#16497=DIRECTION('',(0.,-1.,0.));
#16498=DIRECTION('',(1.,0.,1.20185167898973E-16));
#16499=DIRECTION('center_axis',(-0.866025403784439,0.,-0.5));
#16500=DIRECTION('ref_axis',(0.5,0.,-0.866025403784439));
#16501=DIRECTION('',(-0.5,0.,0.866025403784439));
#16502=DIRECTION('',(0.,-1.,0.));
#16503=DIRECTION('',(0.5,0.,-0.866025403784439));
#16504=DIRECTION('center_axis',(-0.866025403784439,0.,0.5));
#16505=DIRECTION('ref_axis',(-0.5,0.,-0.866025403784439));
#16506=DIRECTION('',(0.5,0.,0.866025403784439));
#16507=DIRECTION('',(0.,-1.,0.));
#16508=DIRECTION('',(-0.5,0.,-0.866025403784439));
#16509=DIRECTION('center_axis',(-2.40370335797945E-16,0.,1.));
#16510=DIRECTION('ref_axis',(-1.,0.,-2.40370335797945E-16));
#16511=DIRECTION('',(1.,0.,2.40370335797945E-16));
#16512=DIRECTION('',(0.,-1.,0.));
#16513=DIRECTION('',(-1.,0.,-2.40370335797945E-16));
#16514=DIRECTION('center_axis',(0.866025403784439,0.,0.5));
#16515=DIRECTION('ref_axis',(-0.5,0.,0.866025403784439));
#16516=DIRECTION('',(0.5,0.,-0.866025403784439));
#16517=DIRECTION('',(-0.5,0.,0.866025403784439));
#16518=DIRECTION('center_axis',(0.,1.,0.));
#16519=DIRECTION('ref_axis',(1.,0.,0.));
#16520=DIRECTION('center_axis',(0.,-1.,0.));
#16521=DIRECTION('ref_axis',(0.,0.,-1.));
#16522=DIRECTION('center_axis',(0.,1.,0.));
#16523=DIRECTION('ref_axis',(1.,0.,0.));
#16524=DIRECTION('center_axis',(0.,1.,0.));
#16525=DIRECTION('ref_axis',(1.,0.,0.));
#16526=DIRECTION('center_axis',(0.,1.,0.));
#16527=DIRECTION('ref_axis',(0.,0.,1.));
#16528=DIRECTION('center_axis',(0.,-1.,0.));
#16529=DIRECTION('ref_axis',(1.,0.,0.));
#16530=DIRECTION('center_axis',(0.,-1.,0.));
#16531=DIRECTION('ref_axis',(1.,0.,0.));
#16532=DIRECTION('center_axis',(0.,-1.,0.));
#16533=DIRECTION('ref_axis',(1.,0.,0.));
#16534=DIRECTION('',(0.707106781186548,0.707106781186547,8.65956056235493E-17));
#16535=DIRECTION('center_axis',(0.,-1.,0.));
#16536=DIRECTION('ref_axis',(1.,0.,0.));
#16537=DIRECTION('center_axis',(0.,-1.,0.));
#16538=DIRECTION('ref_axis',(1.,0.,0.));
#16539=DIRECTION('',(0.,1.,0.));
#16540=DIRECTION('center_axis',(0.,1.,0.));
#16541=DIRECTION('ref_axis',(1.,0.,0.));
#16542=DIRECTION('center_axis',(0.,-1.,0.));
#16543=DIRECTION('ref_axis',(1.,0.,0.));
#16544=DIRECTION('',(-0.707106781186547,0.707106781186548,-8.65956056235493E-17));
#16545=DIRECTION('center_axis',(0.,-1.,0.));
#16546=DIRECTION('ref_axis',(0.,0.,-1.));
#16547=DIRECTION('center_axis',(0.,-1.,0.));
#16548=DIRECTION('ref_axis',(1.,0.,0.));
#16549=DIRECTION('center_axis',(0.,1.,0.));
#16550=DIRECTION('ref_axis',(1.,0.,0.));
#16551=DIRECTION('center_axis',(0.,1.,0.));
#16552=DIRECTION('ref_axis',(1.,0.,0.));
#16553=DIRECTION('',(-0.447213595499958,0.894427190999916,-5.47678698264203E-17));
#16554=DIRECTION('center_axis',(0.,-1.,0.));
#16555=DIRECTION('ref_axis',(1.,0.,0.));
#16556=DIRECTION('',(0.,1.,0.));
#20783=CARTESIAN_POINT('',(0.,0.,0.));
#20784=CARTESIAN_POINT('Origin',(0.115470053837925,-0.5,-0.2));
#20785=CARTESIAN_POINT('',(0.23094010767585,-0.5,0.));
#20786=CARTESIAN_POINT('',(0.115470053837925,-0.5,-0.2));
#20787=CARTESIAN_POINT('',(0.23094010767585,-0.5,0.));
#20788=CARTESIAN_POINT('',(0.115470053837925,-0.8,-0.2));
#20789=CARTESIAN_POINT('',(0.115470053837925,-0.5,-0.2));
#20790=CARTESIAN_POINT('',(0.23094010767585,-0.8,0.));
#20791=CARTESIAN_POINT('',(0.23094010767585,-0.8,0.));
#20792=CARTESIAN_POINT('',(0.23094010767585,-0.5,0.));
#20793=CARTESIAN_POINT('Origin',(-0.115470053837925,-0.5,-0.2));
#20794=CARTESIAN_POINT('',(-0.115470053837925,-0.5,-0.2));
#20795=CARTESIAN_POINT('',(0.115470053837925,-0.5,-0.2));
#20796=CARTESIAN_POINT('',(-0.115470053837925,-0.8,-0.2));
#20797=CARTESIAN_POINT('',(-0.115470053837925,-0.5,-0.2));
#20798=CARTESIAN_POINT('',(0.115470053837925,-0.8,-0.2));
#20799=CARTESIAN_POINT('Origin',(-0.23094010767585,-0.5,-2.77555756156289E-17));
#20800=CARTESIAN_POINT('',(-0.23094010767585,-0.5,-2.82820063659975E-17));
#20801=CARTESIAN_POINT('',(-0.115470053837925,-0.5,-0.2));
#20802=CARTESIAN_POINT('',(-0.23094010767585,-0.8,-2.77555756156289E-17));
#20803=CARTESIAN_POINT('',(-0.23094010767585,-0.5,-2.82820063659975E-17));
#20804=CARTESIAN_POINT('',(-0.115470053837925,-0.8,-0.2));
#20805=CARTESIAN_POINT('Origin',(-0.115470053837925,-0.5,0.2));
#20806=CARTESIAN_POINT('',(-0.115470053837925,-0.5,0.2));
#20807=CARTESIAN_POINT('',(-0.23094010767585,-0.5,-2.82820063659975E-17));
#20808=CARTESIAN_POINT('',(-0.115470053837925,-0.8,0.2));
#20809=CARTESIAN_POINT('',(-0.115470053837925,-0.5,0.2));
#20810=CARTESIAN_POINT('',(-0.23094010767585,-0.8,-2.82820063659975E-17));
#20811=CARTESIAN_POINT('Origin',(0.115470053837925,-0.5,0.2));
#20812=CARTESIAN_POINT('',(0.115470053837925,-0.5,0.2));
#20813=CARTESIAN_POINT('',(-0.115470053837925,-0.5,0.2));
#20814=CARTESIAN_POINT('',(0.115470053837925,-0.8,0.2));
#20815=CARTESIAN_POINT('',(0.115470053837925,-0.5,0.2));
#20816=CARTESIAN_POINT('',(-0.115470053837925,-0.8,0.2));
#20817=CARTESIAN_POINT('Origin',(0.23094010767585,-0.5,0.));
#20818=CARTESIAN_POINT('',(0.115470053837925,-0.5,0.2));
#20819=CARTESIAN_POINT('',(0.115470053837925,-0.8,0.2));
#20820=CARTESIAN_POINT('Origin',(0.,-0.5,0.));
#20821=CARTESIAN_POINT('Origin',(0.,-0.8,0.));
#20822=CARTESIAN_POINT('Origin',(0.,-1.4,0.));
#20823=CARTESIAN_POINT('',(-0.24505,-1.4,3.00099698131059E-17));
#20824=CARTESIAN_POINT('Origin',(0.,-1.4,0.));
#20825=CARTESIAN_POINT('Origin',(0.375,0.5,0.));
#20826=CARTESIAN_POINT('',(-0.375,0.5,-4.59242549680257E-17));
#20827=CARTESIAN_POINT('Origin',(0.,0.5,0.));
#20828=CARTESIAN_POINT('Origin',(0.,0.475,0.));
#20829=CARTESIAN_POINT('',(-0.425,0.45,-5.20474889637625E-17));
#20830=CARTESIAN_POINT('Origin',(0.,0.45,0.));
#20831=CARTESIAN_POINT('',(-0.4,0.475,-4.89858719658941E-17));
#20832=CARTESIAN_POINT('Origin',(0.,0.24,0.));
#20833=CARTESIAN_POINT('',(-0.425,0.0299999999999998,-5.20474889637625E-17));
#20834=CARTESIAN_POINT('Origin',(0.,0.0299999999999998,0.));
#20835=CARTESIAN_POINT('',(-0.425,0.24,-5.20474889637625E-17));
#20836=CARTESIAN_POINT('Origin',(0.,0.0150000000000001,0.));
#20837=CARTESIAN_POINT('',(-0.395,4.85722573273506E-17,-4.83735485663204E-17));
#20838=CARTESIAN_POINT('Origin',(0.,0.,0.));
#20839=CARTESIAN_POINT('',(-0.41,0.0150000000000001,-5.02105187650415E-17));
#20840=CARTESIAN_POINT('Origin',(0.27,0.,0.));
#20841=CARTESIAN_POINT('',(-0.27,0.,-3.30654635769785E-17));
#20842=CARTESIAN_POINT('Origin',(0.,0.,0.));
#20843=CARTESIAN_POINT('Origin',(0.,-0.02,0.));
#20844=CARTESIAN_POINT('',(-0.24505,-0.0498999999999999,3.00099698131059E-17));
#20845=CARTESIAN_POINT('Origin',(0.,-0.0498999999999999,0.));
#20846=CARTESIAN_POINT('',(-0.26,-0.02,-3.18408167778312E-17));
#20847=CARTESIAN_POINT('Origin',(0.,-0.995,0.));
#20848=CARTESIAN_POINT('',(-0.24505,-0.995,-3.00099698131059E-17));
#23493=UNCERTAINTY_MEASURE_WITH_UNIT(LENGTH_MEASURE(0.001),#23588,
'DISTANCE_ACCURACY_VALUE',
'Maximum model space distance between geometric entities at asserted c
onnectivities');
#23522=UNCERTAINTY_MEASURE_WITH_UNIT(LENGTH_MEASURE(0.001),#23588,
'DISTANCE_ACCURACY_VALUE',
'Maximum model space distance between geometric entities at asserted c
onnectivities');
#23558=(
GEOMETRIC_REPRESENTATION_CONTEXT(3)
GLOBAL_UNCERTAINTY_ASSIGNED_CONTEXT((#23493))
GLOBAL_UNIT_ASSIGNED_CONTEXT((#23588,#23590,#23591))
REPRESENTATION_CONTEXT('','3D')
);
#23587=(
GEOMETRIC_REPRESENTATION_CONTEXT(3)
GLOBAL_UNCERTAINTY_ASSIGNED_CONTEXT((#23522))
GLOBAL_UNIT_ASSIGNED_CONTEXT((#23588,#23590,#23591))
REPRESENTATION_CONTEXT('','3D')
);
#23588=(
LENGTH_UNIT()
NAMED_UNIT(*)
SI_UNIT(.CENTI.,.METRE.)
);
#23590=(
NAMED_UNIT(*)
PLANE_ANGLE_UNIT()
SI_UNIT($,.RADIAN.)
);
#23591=(
NAMED_UNIT(*)
SI_UNIT($,.STERADIAN.)
SOLID_ANGLE_UNIT()
);
#23627=SHAPE_DEFINITION_REPRESENTATION(#23699,#23860);
#23699=PRODUCT_DEFINITION_SHAPE('',$,#23925);
#23860=SHAPE_REPRESENTATION('',(#13629),#23558);
#23889=PRODUCT_DEFINITION_CONTEXT('part definition',#24083,'design');
#23925=PRODUCT_DEFINITION('M5x14 Cap Screw','M5x14 Cap Screw',#23989,#23889);
#23989=PRODUCT_DEFINITION_FORMATION('',$,#24120);
#24083=APPLICATION_CONTEXT(
'Core Data for Automotive Mechanical Design Process');
#24084=PRODUCT_CONTEXT('part definition',#24083,'mechanical');
#24120=PRODUCT('M5x14 Cap Screw','M5x14 Cap Screw','M5x14 Cap Screw',(#24084));
#24212=COLOUR_RGB('Black',0.12,0.14,0.17);
#24213=FILL_AREA_STYLE_COLOUR('',#24212);
#24214=FILL_AREA_STYLE('',(#24213));
#24215=SURFACE_STYLE_FILL_AREA(#24214);
#24216=SURFACE_SIDE_STYLE('',(#24215));
#24217=SURFACE_STYLE_USAGE(.BOTH.,#24216);
#24218=PRESENTATION_STYLE_ASSIGNMENT((#24217));
ENDSEC;
END-ISO-10303-21;
